ISO-10303-21;
HEADER;
/* Generated by software containing ST-Developer
 * from STEP Tools, Inc. (www.steptools.com) 
 */

FILE_DESCRIPTION(
/* description */ (''),
/* implementation_level */ '2;1');

FILE_NAME(
/* name */ 'Screw_02.step',
/* time_stamp */ '2026-10-04T22:47:03-07:00',
/* author */ (''),
/* organization */ (''),
/* preprocessor_version */ 'ST-DEVELOPER v20.2',
/* originating_system */ 'Autodesk Translation Framework v15.15.0.0',
/* authorisation */ '');

FILE_SCHEMA (('AUTOMOTIVE_DESIGN { 1 0 10303 214 3 1 1 }'));
ENDSEC;

DATA;
#10=MECHANICAL_DESIGN_GEOMETRIC_PRESENTATION_REPRESENTATION('',(#78),#19878);
#43=TOROIDAL_SURFACE('',#5201,8.911,1.);
#57=CONICAL_SURFACE('',#5198,7.28,0.832981266674429);
#58=CONICAL_SURFACE('',#5205,11.24,0.785398163397495);
#64=SHAPE_REPRESENTATION_RELATIONSHIP('SRR','None',#19908,#71);
#71=ADVANCED_BREP_SHAPE_REPRESENTATION('',(#85),#19872);
#78=STYLED_ITEM('',(#19952),#85);
#85=MANIFOLD_SOLID_BREP('Body1',#4826);
#93=FACE_BOUND('',#783,.T.);
#273=PLANE('',#5208);
#274=PLANE('',#5209);
#275=PLANE('',#5210);
#276=PLANE('',#5211);
#277=PLANE('',#5212);
#278=PLANE('',#5213);
#279=PLANE('',#5214);
#280=PLANE('',#5215);
#281=PLANE('',#5216);
#282=PLANE('',#5217);
#283=PLANE('',#5218);
#284=PLANE('',#5219);
#285=PLANE('',#5220);
#286=PLANE('',#5223);
#488=FACE_OUTER_BOUND('',#766,.T.);
#489=FACE_OUTER_BOUND('',#767,.T.);
#490=FACE_OUTER_BOUND('',#768,.T.);
#491=FACE_OUTER_BOUND('',#769,.T.);
#492=FACE_OUTER_BOUND('',#770,.T.);
#493=FACE_OUTER_BOUND('',#771,.T.);
#494=FACE_OUTER_BOUND('',#772,.T.);
#495=FACE_OUTER_BOUND('',#773,.T.);
#496=FACE_OUTER_BOUND('',#774,.T.);
#497=FACE_OUTER_BOUND('',#775,.T.);
#498=FACE_OUTER_BOUND('',#776,.T.);
#499=FACE_OUTER_BOUND('',#777,.T.);
#500=FACE_OUTER_BOUND('',#778,.T.);
#501=FACE_OUTER_BOUND('',#779,.T.);
#502=FACE_OUTER_BOUND('',#780,.T.);
#503=FACE_OUTER_BOUND('',#781,.T.);
#504=FACE_OUTER_BOUND('',#782,.T.);
#505=FACE_OUTER_BOUND('',#784,.T.);
#506=FACE_OUTER_BOUND('',#785,.T.);
#766=EDGE_LOOP('',(#3993,#3994,#3995,#3996));
#767=EDGE_LOOP('',(#3997,#3998,#3999,#4000));
#768=EDGE_LOOP('',(#4001,#4002,#4003,#4004));
#769=EDGE_LOOP('',(#4005,#4006,#4007,#4008));
#770=EDGE_LOOP('',(#4009,#4010,#4011));
#771=EDGE_LOOP('',(#4012,#4013,#4014));
#772=EDGE_LOOP('',(#4015,#4016,#4017));
#773=EDGE_LOOP('',(#4018,#4019,#4020));
#774=EDGE_LOOP('',(#4021,#4022,#4023));
#775=EDGE_LOOP('',(#4024,#4025,#4026));
#776=EDGE_LOOP('',(#4027,#4028,#4029,#4030));
#777=EDGE_LOOP('',(#4031,#4032,#4033,#4034));
#778=EDGE_LOOP('',(#4035,#4036,#4037,#4038));
#779=EDGE_LOOP('',(#4039,#4040,#4041,#4042));
#780=EDGE_LOOP('',(#4043,#4044,#4045,#4046));
#781=EDGE_LOOP('',(#4047,#4048,#4049,#4050));
#782=EDGE_LOOP('',(#4051));
#783=EDGE_LOOP('',(#4052,#4053,#4054,#4055,#4056,#4057));
#784=EDGE_LOOP('',(#4058,#4059,#4060,#4061));
#785=EDGE_LOOP('',(#4062));
#1138=LINE('',#19393,#1494);
#1139=LINE('',#19404,#1495);
#1140=LINE('',#19406,#1496);
#1141=LINE('',#19410,#1497);
#1142=LINE('',#19412,#1498);
#1143=LINE('',#19413,#1499);
#1144=LINE('',#19416,#1500);
#1145=LINE('',#19417,#1501);
#1146=LINE('',#19420,#1502);
#1147=LINE('',#19421,#1503);
#1148=LINE('',#19424,#1504);
#1149=LINE('',#19425,#1505);
#1150=LINE('',#19428,#1506);
#1151=LINE('',#19429,#1507);
#1152=LINE('',#19431,#1508);
#1153=LINE('',#19435,#1509);
#1154=LINE('',#19436,#1510);
#1155=LINE('',#19437,#1511);
#1156=LINE('',#19440,#1512);
#1157=LINE('',#19441,#1513);
#1158=LINE('',#19444,#1514);
#1159=LINE('',#19445,#1515);
#1160=LINE('',#19448,#1516);
#1161=LINE('',#19449,#1517);
#1162=LINE('',#19452,#1518);
#1163=LINE('',#19453,#1519);
#1164=LINE('',#19455,#1520);
#1165=LINE('',#19460,#1521);
#1494=VECTOR('',#6248,7.28);
#1495=VECTOR('',#6263,11.24);
#1496=VECTOR('',#6266,7.911);
#1497=VECTOR('',#6269,10.);
#1498=VECTOR('',#6270,10.);
#1499=VECTOR('',#6271,10.);
#1500=VECTOR('',#6274,10.);
#1501=VECTOR('',#6275,10.);
#1502=VECTOR('',#6278,10.);
#1503=VECTOR('',#6279,10.);
#1504=VECTOR('',#6282,9.99999999999999);
#1505=VECTOR('',#6283,10.);
#1506=VECTOR('',#6286,10.);
#1507=VECTOR('',#6287,10.);
#1508=VECTOR('',#6290,10.);
#1509=VECTOR('',#6293,10.);
#1510=VECTOR('',#6294,10.);
#1511=VECTOR('',#6295,10.);
#1512=VECTOR('',#6298,10.);
#1513=VECTOR('',#6299,10.);
#1514=VECTOR('',#6302,10.);
#1515=VECTOR('',#6303,10.);
#1516=VECTOR('',#6306,9.99999999999999);
#1517=VECTOR('',#6307,10.);
#1518=VECTOR('',#6310,10.);
#1519=VECTOR('',#6311,10.);
#1520=VECTOR('',#6314,10.);
#1521=VECTOR('',#6321,14.48);
#1771=CIRCLE('',#5199,7.911);
#1772=CIRCLE('',#5200,6.4);
#1773=CIRCLE('',#5202,7.911);
#1774=CIRCLE('',#5203,1.);
#1775=CIRCLE('',#5204,8.20389321881349);
#1776=CIRCLE('',#5206,14.48);
#1777=CIRCLE('',#5221,14.48);
#2197=VERTEX_POINT('',#19390);
#2198=VERTEX_POINT('',#19392);
#2199=VERTEX_POINT('',#19396);
#2200=VERTEX_POINT('',#19398);
#2201=VERTEX_POINT('',#19402);
#2202=VERTEX_POINT('',#19408);
#2203=VERTEX_POINT('',#19409);
#2204=VERTEX_POINT('',#19411);
#2205=VERTEX_POINT('',#19415);
#2206=VERTEX_POINT('',#19419);
#2207=VERTEX_POINT('',#19423);
#2208=VERTEX_POINT('',#19427);
#2209=VERTEX_POINT('',#19433);
#2210=VERTEX_POINT('',#19434);
#2211=VERTEX_POINT('',#19439);
#2212=VERTEX_POINT('',#19443);
#2213=VERTEX_POINT('',#19447);
#2214=VERTEX_POINT('',#19451);
#2215=VERTEX_POINT('',#19457);
#2808=EDGE_CURVE('',#2197,#2197,#1771,.T.);
#2809=EDGE_CURVE('',#2197,#2198,#1138,.T.);
#2810=EDGE_CURVE('',#2198,#2198,#1772,.T.);
#2811=EDGE_CURVE('',#2199,#2199,#1773,.T.);
#2812=EDGE_CURVE('',#2199,#2200,#1774,.T.);
#2813=EDGE_CURVE('',#2200,#2200,#1775,.T.);
#2814=EDGE_CURVE('',#2201,#2201,#1776,.T.);
#2815=EDGE_CURVE('',#2201,#2200,#1139,.T.);
#2816=EDGE_CURVE('',#2197,#2199,#1140,.T.);
#2817=EDGE_CURVE('',#2202,#2203,#1141,.T.);
#2818=EDGE_CURVE('',#2204,#2202,#1142,.T.);
#2819=EDGE_CURVE('',#2204,#2203,#1143,.T.);
#2820=EDGE_CURVE('',#2205,#2204,#1144,.T.);
#2821=EDGE_CURVE('',#2205,#2203,#1145,.T.);
#2822=EDGE_CURVE('',#2206,#2205,#1146,.T.);
#2823=EDGE_CURVE('',#2206,#2203,#1147,.T.);
#2824=EDGE_CURVE('',#2207,#2206,#1148,.T.);
#2825=EDGE_CURVE('',#2207,#2203,#1149,.T.);
#2826=EDGE_CURVE('',#2208,#2207,#1150,.T.);
#2827=EDGE_CURVE('',#2208,#2203,#1151,.T.);
#2828=EDGE_CURVE('',#2202,#2208,#1152,.T.);
#2829=EDGE_CURVE('',#2209,#2210,#1153,.T.);
#2830=EDGE_CURVE('',#2209,#2204,#1154,.T.);
#2831=EDGE_CURVE('',#2210,#2202,#1155,.T.);
#2832=EDGE_CURVE('',#2211,#2209,#1156,.T.);
#2833=EDGE_CURVE('',#2211,#2205,#1157,.T.);
#2834=EDGE_CURVE('',#2212,#2211,#1158,.T.);
#2835=EDGE_CURVE('',#2212,#2206,#1159,.T.);
#2836=EDGE_CURVE('',#2213,#2212,#1160,.T.);
#2837=EDGE_CURVE('',#2213,#2207,#1161,.T.);
#2838=EDGE_CURVE('',#2214,#2213,#1162,.T.);
#2839=EDGE_CURVE('',#2214,#2208,#1163,.T.);
#2840=EDGE_CURVE('',#2210,#2214,#1164,.T.);
#2841=EDGE_CURVE('',#2215,#2215,#1777,.T.);
#2842=EDGE_CURVE('',#2201,#2215,#1165,.T.);
#3993=ORIENTED_EDGE('',*,*,#2808,.F.);
#3994=ORIENTED_EDGE('',*,*,#2809,.T.);
#3995=ORIENTED_EDGE('',*,*,#2810,.F.);
#3996=ORIENTED_EDGE('',*,*,#2809,.F.);
#3997=ORIENTED_EDGE('',*,*,#2811,.T.);
#3998=ORIENTED_EDGE('',*,*,#2812,.T.);
#3999=ORIENTED_EDGE('',*,*,#2813,.T.);
#4000=ORIENTED_EDGE('',*,*,#2812,.F.);
#4001=ORIENTED_EDGE('',*,*,#2814,.T.);
#4002=ORIENTED_EDGE('',*,*,#2815,.T.);
#4003=ORIENTED_EDGE('',*,*,#2813,.F.);
#4004=ORIENTED_EDGE('',*,*,#2815,.F.);
#4005=ORIENTED_EDGE('',*,*,#2808,.T.);
#4006=ORIENTED_EDGE('',*,*,#2816,.T.);
#4007=ORIENTED_EDGE('',*,*,#2811,.F.);
#4008=ORIENTED_EDGE('',*,*,#2816,.F.);
#4009=ORIENTED_EDGE('',*,*,#2817,.F.);
#4010=ORIENTED_EDGE('',*,*,#2818,.F.);
#4011=ORIENTED_EDGE('',*,*,#2819,.T.);
#4012=ORIENTED_EDGE('',*,*,#2819,.F.);
#4013=ORIENTED_EDGE('',*,*,#2820,.F.);
#4014=ORIENTED_EDGE('',*,*,#2821,.T.);
#4015=ORIENTED_EDGE('',*,*,#2821,.F.);
#4016=ORIENTED_EDGE('',*,*,#2822,.F.);
#4017=ORIENTED_EDGE('',*,*,#2823,.T.);
#4018=ORIENTED_EDGE('',*,*,#2823,.F.);
#4019=ORIENTED_EDGE('',*,*,#2824,.F.);
#4020=ORIENTED_EDGE('',*,*,#2825,.T.);
#4021=ORIENTED_EDGE('',*,*,#2825,.F.);
#4022=ORIENTED_EDGE('',*,*,#2826,.F.);
#4023=ORIENTED_EDGE('',*,*,#2827,.T.);
#4024=ORIENTED_EDGE('',*,*,#2827,.F.);
#4025=ORIENTED_EDGE('',*,*,#2828,.F.);
#4026=ORIENTED_EDGE('',*,*,#2817,.T.);
#4027=ORIENTED_EDGE('',*,*,#2829,.F.);
#4028=ORIENTED_EDGE('',*,*,#2830,.T.);
#4029=ORIENTED_EDGE('',*,*,#2818,.T.);
#4030=ORIENTED_EDGE('',*,*,#2831,.F.);
#4031=ORIENTED_EDGE('',*,*,#2832,.F.);
#4032=ORIENTED_EDGE('',*,*,#2833,.T.);
#4033=ORIENTED_EDGE('',*,*,#2820,.T.);
#4034=ORIENTED_EDGE('',*,*,#2830,.F.);
#4035=ORIENTED_EDGE('',*,*,#2834,.F.);
#4036=ORIENTED_EDGE('',*,*,#2835,.T.);
#4037=ORIENTED_EDGE('',*,*,#2822,.T.);
#4038=ORIENTED_EDGE('',*,*,#2833,.F.);
#4039=ORIENTED_EDGE('',*,*,#2836,.F.);
#4040=ORIENTED_EDGE('',*,*,#2837,.T.);
#4041=ORIENTED_EDGE('',*,*,#2824,.T.);
#4042=ORIENTED_EDGE('',*,*,#2835,.F.);
#4043=ORIENTED_EDGE('',*,*,#2838,.F.);
#4044=ORIENTED_EDGE('',*,*,#2839,.T.);
#4045=ORIENTED_EDGE('',*,*,#2826,.T.);
#4046=ORIENTED_EDGE('',*,*,#2837,.F.);
#4047=ORIENTED_EDGE('',*,*,#2840,.F.);
#4048=ORIENTED_EDGE('',*,*,#2831,.T.);
#4049=ORIENTED_EDGE('',*,*,#2828,.T.);
#4050=ORIENTED_EDGE('',*,*,#2839,.F.);
#4051=ORIENTED_EDGE('',*,*,#2841,.F.);
#4052=ORIENTED_EDGE('',*,*,#2829,.T.);
#4053=ORIENTED_EDGE('',*,*,#2840,.T.);
#4054=ORIENTED_EDGE('',*,*,#2838,.T.);
#4055=ORIENTED_EDGE('',*,*,#2836,.T.);
#4056=ORIENTED_EDGE('',*,*,#2834,.T.);
#4057=ORIENTED_EDGE('',*,*,#2832,.T.);
#4058=ORIENTED_EDGE('',*,*,#2814,.F.);
#4059=ORIENTED_EDGE('',*,*,#2842,.T.);
#4060=ORIENTED_EDGE('',*,*,#2841,.T.);
#4061=ORIENTED_EDGE('',*,*,#2842,.F.);
#4062=ORIENTED_EDGE('',*,*,#2810,.T.);
#4512=CYLINDRICAL_SURFACE('',#5207,7.911);
#4513=CYLINDRICAL_SURFACE('',#5222,14.48);
#4712=ADVANCED_FACE('',(#488),#57,.T.);
#4713=ADVANCED_FACE('',(#489),#43,.F.);
#4714=ADVANCED_FACE('',(#490),#58,.T.);
#4715=ADVANCED_FACE('',(#491),#4512,.T.);
#4716=ADVANCED_FACE('',(#492),#273,.F.);
#4717=ADVANCED_FACE('',(#493),#274,.F.);
#4718=ADVANCED_FACE('',(#494),#275,.F.);
#4719=ADVANCED_FACE('',(#495),#276,.F.);
#4720=ADVANCED_FACE('',(#496),#277,.F.);
#4721=ADVANCED_FACE('',(#497),#278,.F.);
#4722=ADVANCED_FACE('',(#498),#279,.F.);
#4723=ADVANCED_FACE('',(#499),#280,.F.);
#4724=ADVANCED_FACE('',(#500),#281,.F.);
#4725=ADVANCED_FACE('',(#501),#282,.F.);
#4726=ADVANCED_FACE('',(#502),#283,.F.);
#4727=ADVANCED_FACE('',(#503),#284,.F.);
#4728=ADVANCED_FACE('',(#504,#93),#285,.T.);
#4729=ADVANCED_FACE('',(#505),#4513,.T.);
#4730=ADVANCED_FACE('',(#506),#286,.T.);
#4826=CLOSED_SHELL('',(#4712,#4713,#4714,#4715,#4716,#4717,#4718,#4719,
#4720,#4721,#4722,#4723,#4724,#4725,#4726,#4727,#4728,#4729,#4730));
#5197=AXIS2_PLACEMENT_3D('',#19388,#6242,#6243);
#5198=AXIS2_PLACEMENT_3D('',#19389,#6244,#6245);
#5199=AXIS2_PLACEMENT_3D('',#19391,#6246,#6247);
#5200=AXIS2_PLACEMENT_3D('',#19394,#6249,#6250);
#5201=AXIS2_PLACEMENT_3D('',#19395,#6251,#6252);
#5202=AXIS2_PLACEMENT_3D('',#19397,#6253,#6254);
#5203=AXIS2_PLACEMENT_3D('',#19399,#6255,#6256);
#5204=AXIS2_PLACEMENT_3D('',#19400,#6257,#6258);
#5205=AXIS2_PLACEMENT_3D('',#19401,#6259,#6260);
#5206=AXIS2_PLACEMENT_3D('',#19403,#6261,#6262);
#5207=AXIS2_PLACEMENT_3D('',#19405,#6264,#6265);
#5208=AXIS2_PLACEMENT_3D('',#19407,#6267,#6268);
#5209=AXIS2_PLACEMENT_3D('',#19414,#6272,#6273);
#5210=AXIS2_PLACEMENT_3D('',#19418,#6276,#6277);
#5211=AXIS2_PLACEMENT_3D('',#19422,#6280,#6281);
#5212=AXIS2_PLACEMENT_3D('',#19426,#6284,#6285);
#5213=AXIS2_PLACEMENT_3D('',#19430,#6288,#6289);
#5214=AXIS2_PLACEMENT_3D('',#19432,#6291,#6292);
#5215=AXIS2_PLACEMENT_3D('',#19438,#6296,#6297);
#5216=AXIS2_PLACEMENT_3D('',#19442,#6300,#6301);
#5217=AXIS2_PLACEMENT_3D('',#19446,#6304,#6305);
#5218=AXIS2_PLACEMENT_3D('',#19450,#6308,#6309);
#5219=AXIS2_PLACEMENT_3D('',#19454,#6312,#6313);
#5220=AXIS2_PLACEMENT_3D('',#19456,#6315,#6316);
#5221=AXIS2_PLACEMENT_3D('',#19458,#6317,#6318);
#5222=AXIS2_PLACEMENT_3D('',#19459,#6319,#6320);
#5223=AXIS2_PLACEMENT_3D('',#19461,#6322,#6323);
#6242=DIRECTION('axis',(0.,0.,1.));
#6243=DIRECTION('refdir',(1.,0.,0.));
#6244=DIRECTION('center_axis',(-7.86407975776121E-17,0.,1.));
#6245=DIRECTION('ref_axis',(-1.,0.,-7.86407975776121E-17));
#6246=DIRECTION('center_axis',(-7.86407975776121E-17,0.,1.));
#6247=DIRECTION('ref_axis',(-1.,0.,-7.86407975776121E-17));
#6248=DIRECTION('',(-0.739940073395942,-9.06165242445198E-17,-0.672672793996315));
#6249=DIRECTION('center_axis',(7.86407975776121E-17,0.,-1.));
#6250=DIRECTION('ref_axis',(-1.,0.,-7.86407975776121E-17));
#6251=DIRECTION('center_axis',(7.86407975776121E-17,0.,-1.));
#6252=DIRECTION('ref_axis',(-1.,0.,-8.96154192009005E-17));
#6253=DIRECTION('center_axis',(-7.86407975776121E-17,0.,1.));
#6254=DIRECTION('ref_axis',(-1.,0.,-7.86407975776121E-17));
#6255=DIRECTION('center_axis',(1.22464679914735E-16,1.,9.63072010358176E-33));
#6256=DIRECTION('ref_axis',(1.,-1.22464679914735E-16,1.12019274001126E-16));
#6257=DIRECTION('center_axis',(0.,0.,-1.));
#6258=DIRECTION('ref_axis',(-1.,6.12323399573677E-17,0.));
#6259=DIRECTION('center_axis',(-7.86407975776121E-17,0.,1.));
#6260=DIRECTION('ref_axis',(-1.,0.,-7.86407975776121E-17));
#6261=DIRECTION('center_axis',(7.86407975776121E-17,0.,-1.));
#6262=DIRECTION('ref_axis',(1.,0.,7.86407975776121E-17));
#6263=DIRECTION('',(-0.70710678118658,-8.65956056235534E-17,-0.707106781186515));
#6264=DIRECTION('center_axis',(7.86407975776121E-17,0.,-1.));
#6265=DIRECTION('ref_axis',(-1.,0.,-7.86407975776121E-17));
#6266=DIRECTION('',(-7.86407975776121E-17,0.,1.));
#6267=DIRECTION('center_axis',(0.25,0.433012701892219,-0.866025403784439));
#6268=DIRECTION('ref_axis',(0.866025403784439,-0.5,2.49215522988657E-16));
#6269=DIRECTION('',(-0.774596669241483,-0.447213595499958,-0.447213595499958));
#6270=DIRECTION('',(0.866025403784439,-0.5,6.81049284760846E-17));
#6271=DIRECTION('',(-1.1466334093198E-16,-0.894427190999916,-0.447213595499958));
#6272=DIRECTION('center_axis',(-0.25,0.433012701892219,-0.866025403784439));
#6273=DIRECTION('ref_axis',(0.866025403784439,0.5,-1.73385880213439E-16));
#6274=DIRECTION('',(0.866025403784439,0.5,6.81049284760846E-17));
#6275=DIRECTION('',(0.774596669241484,-0.447213595499958,-0.447213595499958));
#6276=DIRECTION('center_axis',(-0.5,-1.92296268638357E-16,-0.866025403784439));
#6277=DIRECTION('ref_axis',(-3.84592537276713E-16,1.,-4.40476560101798E-31));
#6278=DIRECTION('',(-3.84592537276713E-16,1.,-3.02446638738394E-32));
#6279=DIRECTION('',(0.774596669241483,0.447213595499958,-0.447213595499958));
#6280=DIRECTION('center_axis',(-0.25,-0.433012701892219,-0.866025403784439));
#6281=DIRECTION('ref_axis',(-0.866025403784438,0.5,-2.09031490959634E-17));
#6282=DIRECTION('',(-0.866025403784438,0.5,-6.81049284760846E-17));
#6283=DIRECTION('',(6.87980045591882E-16,0.894427190999916,-0.447213595499958));
#6284=DIRECTION('center_axis',(0.25,-0.43301270189222,-0.866025403784438));
#6285=DIRECTION('ref_axis',(-0.866025403784439,-0.499999999999999,-1.78830203614062E-16));
#6286=DIRECTION('',(-0.866025403784439,-0.499999999999999,-6.81049284760846E-17));
#6287=DIRECTION('',(-0.774596669241483,0.447213595499959,-0.447213595499958));
#6288=DIRECTION('center_axis',(0.5,0.,-0.866025403784438));
#6289=DIRECTION('ref_axis',(0.,-1.,0.));
#6290=DIRECTION('',(0.,-1.,0.));
#6291=DIRECTION('center_axis',(0.5,0.866025403784439,5.78241158658936E-17));
#6292=DIRECTION('ref_axis',(0.866025403784439,-0.5,6.81049284760846E-17));
#6293=DIRECTION('',(0.866025403784439,-0.5,6.81049284760818E-17));
#6294=DIRECTION('',(1.15648231731787E-16,0.,-1.));
#6295=DIRECTION('',(1.15648231731787E-16,0.,-1.));
#6296=DIRECTION('center_axis',(-0.5,0.866025403784439,-5.78241158658936E-17));
#6297=DIRECTION('ref_axis',(0.866025403784439,0.5,6.81049284760846E-17));
#6298=DIRECTION('',(0.866025403784439,0.5,6.81049284760818E-17));
#6299=DIRECTION('',(1.15648231731787E-16,0.,-1.));
#6300=DIRECTION('center_axis',(-1.,-3.84592537276713E-16,-1.15648231731787E-16));
#6301=DIRECTION('ref_axis',(-3.84592537276713E-16,1.,-3.02446638738394E-32));
#6302=DIRECTION('',(-3.84592537276713E-16,1.,-3.02446638738382E-32));
#6303=DIRECTION('',(1.15648231731787E-16,0.,-1.));
#6304=DIRECTION('center_axis',(-0.5,-0.866025403784439,-5.78241158658936E-17));
#6305=DIRECTION('ref_axis',(-0.866025403784439,0.5,-6.81049284760847E-17));
#6306=DIRECTION('',(-0.866025403784438,0.5,-6.81049284760818E-17));
#6307=DIRECTION('',(1.15648231731787E-16,0.,-1.));
#6308=DIRECTION('center_axis',(0.499999999999999,-0.866025403784439,5.78241158658935E-17));
#6309=DIRECTION('ref_axis',(-0.866025403784439,-0.499999999999999,-6.81049284760846E-17));
#6310=DIRECTION('',(-0.866025403784439,-0.499999999999999,-6.81049284760819E-17));
#6311=DIRECTION('',(1.15648231731787E-16,0.,-1.));
#6312=DIRECTION('center_axis',(1.,0.,1.15648231731787E-16));
#6313=DIRECTION('ref_axis',(0.,-1.,0.));
#6314=DIRECTION('',(0.,-1.,0.));
#6315=DIRECTION('center_axis',(-7.86407975776121E-17,0.,1.));
#6316=DIRECTION('ref_axis',(1.,0.,7.86407975776121E-17));
#6317=DIRECTION('center_axis',(7.86407975776121E-17,0.,-1.));
#6318=DIRECTION('ref_axis',(1.,0.,7.86407975776121E-17));
#6319=DIRECTION('center_axis',(7.86407975776121E-17,0.,-1.));
#6320=DIRECTION('ref_axis',(-1.,0.,-7.86407975776121E-17));
#6321=DIRECTION('',(-7.86407975776121E-17,0.,1.));
#6322=DIRECTION('center_axis',(7.86407975776121E-17,0.,-1.));
#6323=DIRECTION('ref_axis',(-1.,0.,-7.86407975776121E-17));
#19388=CARTESIAN_POINT('',(0.,0.,0.));
#19389=CARTESIAN_POINT('Origin',(-8.50613908013701E-14,0.,-14.2400000000013));
#19390=CARTESIAN_POINT('',(7.91099999999991,9.68818082805471E-16,-13.6663636363649));
#19391=CARTESIAN_POINT('Origin',(-8.5106502022526E-14,0.,-13.6663636363649));
#19392=CARTESIAN_POINT('',(6.39999999999992,-7.83773951454306E-16,-15.0400000000013));
#19393=CARTESIAN_POINT('',(7.27999999999992,8.91542869779273E-16,-14.2400000000013));
#19394=CARTESIAN_POINT('Origin',(-8.4998478163308E-14,0.,-15.0400000000013));
#19395=CARTESIAN_POINT('Origin',(-8.67707890235993E-14,0.,7.49678643762621));
#19396=CARTESIAN_POINT('',(7.91099999999991,9.68818082805471E-16,7.49678643762622));
#19397=CARTESIAN_POINT('Origin',(-8.67707890235993E-14,0.,7.49678643762621));
#19398=CARTESIAN_POINT('',(8.2038932188134,-2.00937431419332E-15,8.20389321881279));
#19399=CARTESIAN_POINT('Origin',(8.91099999999991,-1.09128276272021E-15,
7.49678643762621));
#19400=CARTESIAN_POINT('Origin',(-8.54871728961371E-14,-5.02343578548331E-16,
8.20389321881279));
#19401=CARTESIAN_POINT('Origin',(-8.70651583236477E-14,0.,11.239999999999));
#19402=CARTESIAN_POINT('',(14.4799999999999,-1.77328856516537E-15,14.4799999999987));
#19403=CARTESIAN_POINT('Origin',(-8.73199545077991E-14,0.,14.4799999999987));
#19404=CARTESIAN_POINT('',(11.2399999999999,1.37650300224163E-15,11.239999999999));
#19405=CARTESIAN_POINT('Origin',(-8.59044201514021E-14,0.,-3.52000000000102));
#19406=CARTESIAN_POINT('',(7.91099999999991,-9.68818082805471E-16,-3.52000000000102));
#19407=CARTESIAN_POINT('Origin',(5.,2.88675134594813,10.1599999999987));
#19408=CARTESIAN_POINT('',(5.,2.88675134594813,10.1599999999987));
#19409=CARTESIAN_POINT('',(2.77555756156289E-15,3.60822483003176E-15,7.2732486540506));
#19410=CARTESIAN_POINT('',(3.99999999999999,2.3094010767585,9.5826497308091));
#19411=CARTESIAN_POINT('',(-5.55111512312578E-16,5.77350269189626,10.1599999999987));
#19412=CARTESIAN_POINT('',(-2.13056424354826E-15,5.77350269189626,10.1599999999987));
#19413=CARTESIAN_POINT('',(-1.66533453693773E-15,4.61880215351701,9.5826497308091));
#19414=CARTESIAN_POINT('Origin',(-5.55111512312578E-16,5.77350269189626,
10.1599999999987));
#19415=CARTESIAN_POINT('',(-5.,2.88675134594813,10.1599999999987));
#19416=CARTESIAN_POINT('',(-5.,2.88675134594813,10.1599999999987));
#19417=CARTESIAN_POINT('',(-4.,2.3094010767585,9.5826497308091));
#19418=CARTESIAN_POINT('Origin',(-5.,2.88675134594813,10.1599999999987));
#19419=CARTESIAN_POINT('',(-5.00000000000001,-2.88675134594812,10.1599999999987));
#19420=CARTESIAN_POINT('',(-5.,-2.88675134594812,10.1599999999987));
#19421=CARTESIAN_POINT('',(-4.,-2.3094010767585,9.5826497308091));
#19422=CARTESIAN_POINT('Origin',(-5.00000000000001,-2.88675134594812,10.1599999999987));
#19423=CARTESIAN_POINT('',(-1.0547118733939E-14,-5.77350269189626,10.1599999999987));
#19424=CARTESIAN_POINT('',(-6.37301395980167E-15,-5.77350269189625,10.1599999999987));
#19425=CARTESIAN_POINT('',(-4.9960036108132E-15,-4.618802153517,9.5826497308091));
#19426=CARTESIAN_POINT('Origin',(-1.0547118733939E-14,-5.77350269189626,
10.1599999999987));
#19427=CARTESIAN_POINT('',(4.99999999999999,-2.88675134594813,10.1599999999987));
#19428=CARTESIAN_POINT('',(4.99999999999999,-2.88675134594813,10.1599999999987));
#19429=CARTESIAN_POINT('',(4.,-2.3094010767585,9.5826497308091));
#19430=CARTESIAN_POINT('Origin',(4.99999999999999,-2.88675134594813,10.1599999999987));
#19431=CARTESIAN_POINT('',(5.,2.88675134594813,10.1599999999987));
#19432=CARTESIAN_POINT('Origin',(-2.03450935938186E-15,5.77350269189626,
14.9599999999987));
#19433=CARTESIAN_POINT('',(-1.17646633176102E-15,5.77350269189626,14.9599999999987));
#19434=CARTESIAN_POINT('',(5.,2.88675134594813,14.9599999999987));
#19435=CARTESIAN_POINT('',(-4.18000000000003,8.18682681710891,14.9599999999987));
#19436=CARTESIAN_POINT('',(-1.17646633176102E-15,5.77350269189626,14.9599999999987));
#19437=CARTESIAN_POINT('',(5.,2.88675134594813,14.9599999999987));
#19438=CARTESIAN_POINT('Origin',(-5.,2.88675134594813,14.9599999999987));
#19439=CARTESIAN_POINT('',(-5.00000000000001,2.88675134594813,14.9599999999987));
#19440=CARTESIAN_POINT('',(-9.18000000000004,0.473427220735475,14.9599999999987));
#19441=CARTESIAN_POINT('',(-5.00000000000001,2.88675134594813,14.9599999999987));
#19442=CARTESIAN_POINT('Origin',(-5.,-2.88675134594812,14.9599999999987));
#19443=CARTESIAN_POINT('',(-5.00000000000001,-2.88675134594812,14.9599999999987));
#19444=CARTESIAN_POINT('',(-5.,-1.44337567297406,14.9599999999987));
#19445=CARTESIAN_POINT('',(-5.00000000000001,-2.88675134594812,14.9599999999987));
#19446=CARTESIAN_POINT('Origin',(-9.14690518987735E-15,-5.77350269189625,
14.9599999999987));
#19447=CARTESIAN_POINT('',(-1.11684735533874E-14,-5.77350269189626,14.9599999999987));
#19448=CARTESIAN_POINT('',(-6.68000000000004,-1.91680289370953,14.9599999999987));
#19449=CARTESIAN_POINT('',(-1.11684735533874E-14,-5.77350269189626,14.9599999999987));
#19450=CARTESIAN_POINT('Origin',(4.99999999999999,-2.88675134594813,14.9599999999987));
#19451=CARTESIAN_POINT('',(4.99999999999999,-2.88675134594813,14.9599999999987));
#19452=CARTESIAN_POINT('',(-1.68000000000005,-6.74345114413485,14.9599999999987));
#19453=CARTESIAN_POINT('',(4.99999999999999,-2.88675134594813,14.9599999999987));
#19454=CARTESIAN_POINT('Origin',(5.,2.88675134594813,14.9599999999987));
#19455=CARTESIAN_POINT('',(5.,1.44337567297406,14.9599999999987));
#19456=CARTESIAN_POINT('Origin',(-14.4800000000001,0.,14.9599999999987));
#19457=CARTESIAN_POINT('',(14.4799999999999,-1.77328856516537E-15,14.9599999999987));
#19458=CARTESIAN_POINT('Origin',(-8.73577020906364E-14,0.,14.9599999999987));
#19459=CARTESIAN_POINT('Origin',(-8.73388282992177E-14,0.,14.7199999999987));
#19460=CARTESIAN_POINT('',(14.4799999999999,-1.77328856516537E-15,14.7199999999987));
#19461=CARTESIAN_POINT('Origin',(-8.54871728961371E-14,0.,-15.0400000000013));
#19863=UNCERTAINTY_MEASURE_WITH_UNIT(LENGTH_MEASURE(0.01),#19879,
'DISTANCE_ACCURACY_VALUE',
'Maximum model space distance between geometric entities at asserted c
onnectivities');
#19869=UNCERTAINTY_MEASURE_WITH_UNIT(LENGTH_MEASURE(0.01),#19879,
'DISTANCE_ACCURACY_VALUE',
'Maximum model space distance between geometric entities at asserted c
onnectivities');
#19872=(
GEOMETRIC_REPRESENTATION_CONTEXT(3)
GLOBAL_UNCERTAINTY_ASSIGNED_CONTEXT((#19863))
GLOBAL_UNIT_ASSIGNED_CONTEXT((#19879,#19881,#19882))
REPRESENTATION_CONTEXT('','3D')
);
#19878=(
GEOMETRIC_REPRESENTATION_CONTEXT(3)
GLOBAL_UNCERTAINTY_ASSIGNED_CONTEXT((#19869))
GLOBAL_UNIT_ASSIGNED_CONTEXT((#19879,#19881,#19882))
REPRESENTATION_CONTEXT('','3D')
);
#19879=(
LENGTH_UNIT()
NAMED_UNIT(*)
SI_UNIT(.MILLI.,.METRE.)
);
#19881=(
NAMED_UNIT(*)
PLANE_ANGLE_UNIT()
SI_UNIT($,.RADIAN.)
);
#19882=(
NAMED_UNIT(*)
SI_UNIT($,.STERADIAN.)
SOLID_ANGLE_UNIT()
);
#19885=SHAPE_DEFINITION_REPRESENTATION(#19893,#19908);
#19893=PRODUCT_DEFINITION_SHAPE('',$,#19917);
#19908=SHAPE_REPRESENTATION('',(#5197),#19872);
#19914=PRODUCT_DEFINITION_CONTEXT('part definition',#19940,'design');
#19917=PRODUCT_DEFINITION(
'BHSFCHCS ANSI B18.3.5M - M16x30 Steel Grade 2 Plain','Screw_02',#19925,
#19914);
#19925=PRODUCT_DEFINITION_FORMATION('',$,#19944);
#19940=APPLICATION_CONTEXT(
'Core Data for Automotive Mechanical Design Process');
#19941=PRODUCT_CONTEXT('part definition',#19940,'mechanical');
#19944=PRODUCT('BHSFCHCS ANSI B18.3.5M - M16x30 Steel Grade 2 Plain',
'Screw_02',
'Broached Hexagon Socket Flat Countersunk Head Cap Screw ANSI B18.3.5M
 - M16x30',(#19941));
#19952=PRESENTATION_STYLE_ASSIGNMENT((#19958));
#19958=SURFACE_STYLE_USAGE(.BOTH.,#19964);
#19964=SURFACE_SIDE_STYLE('',(#19970));
#19970=SURFACE_STYLE_FILL_AREA(#19976);
#19976=FILL_AREA_STYLE('Opaque(160,160,160)',(#19982));
#19982=FILL_AREA_STYLE_COLOUR('Opaque(160,160,160)',#19988);
#19988=COLOUR_RGB('Opaque(160,160,160)', 0.66274510, 0.83137255, 0.94901961);
ENDSEC;
END-ISO-10303-21;
